ISO-10303-21;
HEADER;
/* Generated by software containing ST-Developer
 * from STEP Tools, Inc. (www.steptools.com) 
 */

FILE_DESCRIPTION(
/* description */ ('Flywheel Crank-Slider'),
/* implementation_level */ '2;1');

FILE_NAME(
/* name */ 'Cap Screw - M4x16.step',
/* time_stamp */ '2026-10-28T03:23:13-07:00',
/* author */ (''),
/* organization */ (''),
/* preprocessor_version */ 'ST-DEVELOPER v20.2',
/* originating_system */ 'Autodesk Translation Framework v15.17.0.0',
/* authorisation */ '');

FILE_SCHEMA (('AUTOMOTIVE_DESIGN { 1 0 10303 214 3 1 1 }'));
ENDSEC;

DATA;
#10=MECHANICAL_DESIGN_GEOMETRIC_PRESENTATION_REPRESENTATION('',(#688),#17322);
#532=ORIENTED_CLOSED_SHELL('',*,#9070,.F.);
#545=CONICAL_SURFACE('',#10153,0.325,0.785398163397448);
#546=CONICAL_SURFACE('',#10157,0.335,0.785398163397448);
#547=CONICAL_SURFACE('',#10161,0.21,0.463647609000806);
#548=CONICAL_SURFACE('',#10165,0.18,0.785398163397448);
#562=BREP_WITH_VOIDS('Body1',#9069,(#532));
#583=SHAPE_REPRESENTATION_RELATIONSHIP('SRR','None',#17580,#635);
#635=ADVANCED_BREP_SHAPE_REPRESENTATION('',(#562),#17284);
#688=STYLED_ITEM('',(#17938),#562);
#907=FACE_BOUND('',#2236,.T.);
#1162=PLANE('',#10151);
#1163=PLANE('',#10159);
#1164=PLANE('',#10167);
#1165=PLANE('',#10168);
#1166=PLANE('',#10169);
#1167=PLANE('',#10170);
#1168=PLANE('',#10171);
#1169=PLANE('',#10172);
#1170=PLANE('',#10173);
#1171=PLANE('',#10174);
#1172=PLANE('',#10175);
#1574=FACE_OUTER_BOUND('',#2231,.T.);
#1575=FACE_OUTER_BOUND('',#2232,.T.);
#1576=FACE_OUTER_BOUND('',#2233,.T.);
#1577=FACE_OUTER_BOUND('',#2234,.T.);
#1578=FACE_OUTER_BOUND('',#2235,.T.);
#1579=FACE_OUTER_BOUND('',#2237,.T.);
#1580=FACE_OUTER_BOUND('',#2238,.T.);
#1581=FACE_OUTER_BOUND('',#2239,.T.);
#1582=FACE_OUTER_BOUND('',#2240,.T.);
#1583=FACE_OUTER_BOUND('',#2241,.T.);
#1584=FACE_OUTER_BOUND('',#2242,.T.);
#1585=FACE_OUTER_BOUND('',#2243,.T.);
#1586=FACE_OUTER_BOUND('',#2244,.T.);
#1587=FACE_OUTER_BOUND('',#2245,.T.);
#1588=FACE_OUTER_BOUND('',#2246,.T.);
#1589=FACE_OUTER_BOUND('',#2247,.T.);
#1590=FACE_OUTER_BOUND('',#2248,.T.);
#2231=EDGE_LOOP('',(#7204));
#2232=EDGE_LOOP('',(#7205,#7206,#7207,#7208));
#2233=EDGE_LOOP('',(#7209,#7210,#7211,#7212));
#2234=EDGE_LOOP('',(#7213,#7214,#7215,#7216));
#2235=EDGE_LOOP('',(#7217));
#2236=EDGE_LOOP('',(#7218));
#2237=EDGE_LOOP('',(#7219,#7220,#7221,#7222));
#2238=EDGE_LOOP('',(#7223,#7224,#7225,#7226));
#2239=EDGE_LOOP('',(#7227,#7228,#7229,#7230));
#2240=EDGE_LOOP('',(#7231));
#2241=EDGE_LOOP('',(#7232,#7233,#7234,#7235));
#2242=EDGE_LOOP('',(#7236,#7237,#7238,#7239));
#2243=EDGE_LOOP('',(#7240,#7241,#7242,#7243));
#2244=EDGE_LOOP('',(#7244,#7245,#7246,#7247));
#2245=EDGE_LOOP('',(#7248,#7249,#7250,#7251));
#2246=EDGE_LOOP('',(#7252,#7253,#7254,#7255));
#2247=EDGE_LOOP('',(#7256,#7257,#7258,#7259,#7260,#7261));
#2248=EDGE_LOOP('',(#7262,#7263,#7264,#7265,#7266,#7267));
#2946=LINE('',#15324,#3557);
#2947=LINE('',#15328,#3558);
#2948=LINE('',#15332,#3559);
#2949=LINE('',#15339,#3560);
#2950=LINE('',#15343,#3561);
#2951=LINE('',#15347,#3562);
#2952=LINE('',#15352,#3563);
#2953=LINE('',#15354,#3564);
#2954=LINE('',#15356,#3565);
#2955=LINE('',#15357,#3566);
#2956=LINE('',#15360,#3567);
#2957=LINE('',#15362,#3568);
#2958=LINE('',#15363,#3569);
#2959=LINE('',#15366,#3570);
#2960=LINE('',#15368,#3571);
#2961=LINE('',#15369,#3572);
#2962=LINE('',#15372,#3573);
#2963=LINE('',#15374,#3574);
#2964=LINE('',#15375,#3575);
#2965=LINE('',#15378,#3576);
#2966=LINE('',#15380,#3577);
#2967=LINE('',#15381,#3578);
#2968=LINE('',#15383,#3579);
#2969=LINE('',#15384,#3580);
#3557=VECTOR('',#12100,0.325);
#3558=VECTOR('',#12105,0.35);
#3559=VECTOR('',#12110,0.335);
#3560=VECTOR('',#12119,0.21);
#3561=VECTOR('',#12124,0.2);
#3562=VECTOR('',#12129,0.18);
#3563=VECTOR('',#12134,1.);
#3564=VECTOR('',#12135,1.);
#3565=VECTOR('',#12136,1.);
#3566=VECTOR('',#12137,1.);
#3567=VECTOR('',#12140,1.);
#3568=VECTOR('',#12141,1.);
#3569=VECTOR('',#12142,1.);
#3570=VECTOR('',#12145,1.);
#3571=VECTOR('',#12146,1.);
#3572=VECTOR('',#12147,1.);
#3573=VECTOR('',#12150,1.);
#3574=VECTOR('',#12151,1.);
#3575=VECTOR('',#12152,1.);
#3576=VECTOR('',#12155,1.);
#3577=VECTOR('',#12156,1.);
#3578=VECTOR('',#12157,1.);
#3579=VECTOR('',#12160,1.);
#3580=VECTOR('',#12161,1.);
#4025=CIRCLE('',#10152,0.3);
#4026=CIRCLE('',#10154,0.35);
#4027=CIRCLE('',#10156,0.35);
#4028=CIRCLE('',#10158,0.32);
#4029=CIRCLE('',#10160,0.22);
#4030=CIRCLE('',#10162,0.1954);
#4031=CIRCLE('',#10164,0.1954);
#4032=CIRCLE('',#10166,0.16);
#4636=VERTEX_POINT('',#15319);
#4637=VERTEX_POINT('',#15322);
#4638=VERTEX_POINT('',#15326);
#4639=VERTEX_POINT('',#15330);
#4640=VERTEX_POINT('',#15334);
#4641=VERTEX_POINT('',#15337);
#4642=VERTEX_POINT('',#15341);
#4643=VERTEX_POINT('',#15345);
#4644=VERTEX_POINT('',#15350);
#4645=VERTEX_POINT('',#15351);
#4646=VERTEX_POINT('',#15353);
#4647=VERTEX_POINT('',#15355);
#4648=VERTEX_POINT('',#15359);
#4649=VERTEX_POINT('',#15361);
#4650=VERTEX_POINT('',#15365);
#4651=VERTEX_POINT('',#15367);
#4652=VERTEX_POINT('',#15371);
#4653=VERTEX_POINT('',#15373);
#4654=VERTEX_POINT('',#15377);
#4655=VERTEX_POINT('',#15379);
#5559=EDGE_CURVE('',#4636,#4636,#4025,.T.);
#5560=EDGE_CURVE('',#4637,#4637,#4026,.T.);
#5561=EDGE_CURVE('',#4637,#4636,#2946,.T.);
#5562=EDGE_CURVE('',#4638,#4638,#4027,.T.);
#5563=EDGE_CURVE('',#4638,#4637,#2947,.T.);
#5564=EDGE_CURVE('',#4639,#4639,#4028,.T.);
#5565=EDGE_CURVE('',#4639,#4638,#2948,.T.);
#5566=EDGE_CURVE('',#4640,#4640,#4029,.T.);
#5567=EDGE_CURVE('',#4641,#4641,#4030,.F.);
#5568=EDGE_CURVE('',#4641,#4640,#2949,.T.);
#5569=EDGE_CURVE('',#4642,#4642,#4031,.F.);
#5570=EDGE_CURVE('',#4642,#4641,#2950,.T.);
#5571=EDGE_CURVE('',#4643,#4643,#4032,.T.);
#5572=EDGE_CURVE('',#4643,#4642,#2951,.T.);
#5573=EDGE_CURVE('',#4644,#4645,#2952,.T.);
#5574=EDGE_CURVE('',#4645,#4646,#2953,.T.);
#5575=EDGE_CURVE('',#4646,#4647,#2954,.T.);
#5576=EDGE_CURVE('',#4644,#4647,#2955,.T.);
#5577=EDGE_CURVE('',#4645,#4648,#2956,.T.);
#5578=EDGE_CURVE('',#4648,#4649,#2957,.T.);
#5579=EDGE_CURVE('',#4649,#4646,#2958,.T.);
#5580=EDGE_CURVE('',#4648,#4650,#2959,.T.);
#5581=EDGE_CURVE('',#4650,#4651,#2960,.T.);
#5582=EDGE_CURVE('',#4651,#4649,#2961,.T.);
#5583=EDGE_CURVE('',#4650,#4652,#2962,.T.);
#5584=EDGE_CURVE('',#4652,#4653,#2963,.T.);
#5585=EDGE_CURVE('',#4653,#4651,#2964,.T.);
#5586=EDGE_CURVE('',#4652,#4654,#2965,.T.);
#5587=EDGE_CURVE('',#4654,#4655,#2966,.T.);
#5588=EDGE_CURVE('',#4655,#4653,#2967,.T.);
#5589=EDGE_CURVE('',#4654,#4644,#2968,.T.);
#5590=EDGE_CURVE('',#4647,#4655,#2969,.T.);
#7204=ORIENTED_EDGE('',*,*,#5559,.F.);
#7205=ORIENTED_EDGE('',*,*,#5560,.F.);
#7206=ORIENTED_EDGE('',*,*,#5561,.T.);
#7207=ORIENTED_EDGE('',*,*,#5559,.T.);
#7208=ORIENTED_EDGE('',*,*,#5561,.F.);
#7209=ORIENTED_EDGE('',*,*,#5562,.F.);
#7210=ORIENTED_EDGE('',*,*,#5563,.T.);
#7211=ORIENTED_EDGE('',*,*,#5560,.T.);
#7212=ORIENTED_EDGE('',*,*,#5563,.F.);
#7213=ORIENTED_EDGE('',*,*,#5564,.F.);
#7214=ORIENTED_EDGE('',*,*,#5565,.T.);
#7215=ORIENTED_EDGE('',*,*,#5562,.T.);
#7216=ORIENTED_EDGE('',*,*,#5565,.F.);
#7217=ORIENTED_EDGE('',*,*,#5564,.T.);
#7218=ORIENTED_EDGE('',*,*,#5566,.F.);
#7219=ORIENTED_EDGE('',*,*,#5567,.F.);
#7220=ORIENTED_EDGE('',*,*,#5568,.T.);
#7221=ORIENTED_EDGE('',*,*,#5566,.T.);
#7222=ORIENTED_EDGE('',*,*,#5568,.F.);
#7223=ORIENTED_EDGE('',*,*,#5569,.F.);
#7224=ORIENTED_EDGE('',*,*,#5570,.T.);
#7225=ORIENTED_EDGE('',*,*,#5567,.T.);
#7226=ORIENTED_EDGE('',*,*,#5570,.F.);
#7227=ORIENTED_EDGE('',*,*,#5571,.F.);
#7228=ORIENTED_EDGE('',*,*,#5572,.T.);
#7229=ORIENTED_EDGE('',*,*,#5569,.T.);
#7230=ORIENTED_EDGE('',*,*,#5572,.F.);
#7231=ORIENTED_EDGE('',*,*,#5571,.T.);
#7232=ORIENTED_EDGE('',*,*,#5573,.T.);
#7233=ORIENTED_EDGE('',*,*,#5574,.T.);
#7234=ORIENTED_EDGE('',*,*,#5575,.T.);
#7235=ORIENTED_EDGE('',*,*,#5576,.F.);
#7236=ORIENTED_EDGE('',*,*,#5577,.T.);
#7237=ORIENTED_EDGE('',*,*,#5578,.T.);
#7238=ORIENTED_EDGE('',*,*,#5579,.T.);
#7239=ORIENTED_EDGE('',*,*,#5574,.F.);
#7240=ORIENTED_EDGE('',*,*,#5580,.T.);
#7241=ORIENTED_EDGE('',*,*,#5581,.T.);
#7242=ORIENTED_EDGE('',*,*,#5582,.T.);
#7243=ORIENTED_EDGE('',*,*,#5578,.F.);
#7244=ORIENTED_EDGE('',*,*,#5583,.T.);
#7245=ORIENTED_EDGE('',*,*,#5584,.T.);
#7246=ORIENTED_EDGE('',*,*,#5585,.T.);
#7247=ORIENTED_EDGE('',*,*,#5581,.F.);
#7248=ORIENTED_EDGE('',*,*,#5586,.T.);
#7249=ORIENTED_EDGE('',*,*,#5587,.T.);
#7250=ORIENTED_EDGE('',*,*,#5588,.T.);
#7251=ORIENTED_EDGE('',*,*,#5584,.F.);
#7252=ORIENTED_EDGE('',*,*,#5589,.T.);
#7253=ORIENTED_EDGE('',*,*,#5576,.T.);
#7254=ORIENTED_EDGE('',*,*,#5590,.T.);
#7255=ORIENTED_EDGE('',*,*,#5587,.F.);
#7256=ORIENTED_EDGE('',*,*,#5589,.F.);
#7257=ORIENTED_EDGE('',*,*,#5586,.F.);
#7258=ORIENTED_EDGE('',*,*,#5583,.F.);
#7259=ORIENTED_EDGE('',*,*,#5580,.F.);
#7260=ORIENTED_EDGE('',*,*,#5577,.F.);
#7261=ORIENTED_EDGE('',*,*,#5573,.F.);
#7262=ORIENTED_EDGE('',*,*,#5590,.F.);
#7263=ORIENTED_EDGE('',*,*,#5575,.F.);
#7264=ORIENTED_EDGE('',*,*,#5579,.F.);
#7265=ORIENTED_EDGE('',*,*,#5582,.F.);
#7266=ORIENTED_EDGE('',*,*,#5585,.F.);
#7267=ORIENTED_EDGE('',*,*,#5588,.F.);
#8420=CYLINDRICAL_SURFACE('',#10155,0.35);
#8421=CYLINDRICAL_SURFACE('',#10163,0.1954);
#8765=ADVANCED_FACE('',(#1574),#1162,.T.);
#8766=ADVANCED_FACE('',(#1575),#545,.T.);
#8767=ADVANCED_FACE('',(#1576),#8420,.T.);
#8768=ADVANCED_FACE('',(#1577),#546,.T.);
#8769=ADVANCED_FACE('',(#1578,#907),#1163,.T.);
#8770=ADVANCED_FACE('',(#1579),#547,.T.);
#8771=ADVANCED_FACE('',(#1580),#8421,.T.);
#8772=ADVANCED_FACE('',(#1581),#548,.T.);
#8773=ADVANCED_FACE('',(#1582),#1164,.T.);
#8774=ADVANCED_FACE('',(#1583),#1165,.F.);
#8775=ADVANCED_FACE('',(#1584),#1166,.F.);
#8776=ADVANCED_FACE('',(#1585),#1167,.F.);
#8777=ADVANCED_FACE('',(#1586),#1168,.F.);
#8778=ADVANCED_FACE('',(#1587),#1169,.F.);
#8779=ADVANCED_FACE('',(#1588),#1170,.F.);
#8780=ADVANCED_FACE('',(#1589),#1171,.F.);
#8781=ADVANCED_FACE('',(#1590),#1172,.F.);
#9069=CLOSED_SHELL('',(#8765,#8766,#8767,#8768,#8769,#8770,#8771,#8772,
#8773));
#9070=CLOSED_SHELL('',(#8774,#8775,#8776,#8777,#8778,#8779,#8780,#8781));
#10150=AXIS2_PLACEMENT_3D('',#15317,#12090,#12091);
#10151=AXIS2_PLACEMENT_3D('',#15318,#12092,#12093);
#10152=AXIS2_PLACEMENT_3D('',#15320,#12094,#12095);
#10153=AXIS2_PLACEMENT_3D('',#15321,#12096,#12097);
#10154=AXIS2_PLACEMENT_3D('',#15323,#12098,#12099);
#10155=AXIS2_PLACEMENT_3D('',#15325,#12101,#12102);
#10156=AXIS2_PLACEMENT_3D('',#15327,#12103,#12104);
#10157=AXIS2_PLACEMENT_3D('',#15329,#12106,#12107);
#10158=AXIS2_PLACEMENT_3D('',#15331,#12108,#12109);
#10159=AXIS2_PLACEMENT_3D('',#15333,#12111,#12112);
#10160=AXIS2_PLACEMENT_3D('',#15335,#12113,#12114);
#10161=AXIS2_PLACEMENT_3D('',#15336,#12115,#12116);
#10162=AXIS2_PLACEMENT_3D('',#15338,#12117,#12118);
#10163=AXIS2_PLACEMENT_3D('',#15340,#12120,#12121);
#10164=AXIS2_PLACEMENT_3D('',#15342,#12122,#12123);
#10165=AXIS2_PLACEMENT_3D('',#15344,#12125,#12126);
#10166=AXIS2_PLACEMENT_3D('',#15346,#12127,#12128);
#10167=AXIS2_PLACEMENT_3D('',#15348,#12130,#12131);
#10168=AXIS2_PLACEMENT_3D('',#15349,#12132,#12133);
#10169=AXIS2_PLACEMENT_3D('',#15358,#12138,#12139);
#10170=AXIS2_PLACEMENT_3D('',#15364,#12143,#12144);
#10171=AXIS2_PLACEMENT_3D('',#15370,#12148,#12149);
#10172=AXIS2_PLACEMENT_3D('',#15376,#12153,#12154);
#10173=AXIS2_PLACEMENT_3D('',#15382,#12158,#12159);
#10174=AXIS2_PLACEMENT_3D('',#15385,#12162,#12163);
#10175=AXIS2_PLACEMENT_3D('',#15386,#12164,#12165);
#12090=DIRECTION('axis',(0.,0.,1.));
#12091=DIRECTION('refdir',(1.,0.,0.));
#12092=DIRECTION('center_axis',(0.,1.,0.));
#12093=DIRECTION('ref_axis',(0.,0.,1.));
#12094=DIRECTION('center_axis',(0.,-1.,0.));
#12095=DIRECTION('ref_axis',(1.,0.,0.));
#12096=DIRECTION('center_axis',(0.,-1.,0.));
#12097=DIRECTION('ref_axis',(1.,0.,0.));
#12098=DIRECTION('center_axis',(0.,-1.,0.));
#12099=DIRECTION('ref_axis',(1.,0.,0.));
#12100=DIRECTION('',(0.707106781186547,0.707106781186548,8.65956056235493E-17));
#12101=DIRECTION('center_axis',(0.,-1.,0.));
#12102=DIRECTION('ref_axis',(1.,0.,0.));
#12103=DIRECTION('center_axis',(0.,-1.,0.));
#12104=DIRECTION('ref_axis',(1.,0.,0.));
#12105=DIRECTION('',(0.,1.,0.));
#12106=DIRECTION('center_axis',(0.,1.,0.));
#12107=DIRECTION('ref_axis',(1.,0.,0.));
#12108=DIRECTION('center_axis',(0.,-1.,0.));
#12109=DIRECTION('ref_axis',(1.,0.,0.));
#12110=DIRECTION('',(-0.707106781186547,0.707106781186548,-8.65956056235493E-17));
#12111=DIRECTION('center_axis',(0.,-1.,0.));
#12112=DIRECTION('ref_axis',(0.,0.,-1.));
#12113=DIRECTION('center_axis',(0.,-1.,0.));
#12114=DIRECTION('ref_axis',(1.,0.,0.));
#12115=DIRECTION('center_axis',(0.,1.,0.));
#12116=DIRECTION('ref_axis',(1.,0.,0.));
#12117=DIRECTION('center_axis',(0.,1.,0.));
#12118=DIRECTION('ref_axis',(1.,0.,0.));
#12119=DIRECTION('',(-0.447213595499958,0.894427190999916,-5.47678698264203E-17));
#12120=DIRECTION('center_axis',(0.,-1.,0.));
#12121=DIRECTION('ref_axis',(1.,0.,0.));
#12122=DIRECTION('center_axis',(0.,1.,0.));
#12123=DIRECTION('ref_axis',(1.,0.,0.));
#12124=DIRECTION('',(0.,1.,0.));
#12125=DIRECTION('center_axis',(0.,1.,0.));
#12126=DIRECTION('ref_axis',(1.,0.,0.));
#12127=DIRECTION('center_axis',(0.,-1.,0.));
#12128=DIRECTION('ref_axis',(1.,0.,0.));
#12129=DIRECTION('',(-0.707106781186547,0.707106781186548,-8.65956056235493E-17));
#12130=DIRECTION('center_axis',(0.,-1.,0.));
#12131=DIRECTION('ref_axis',(0.,0.,-1.));
#12132=DIRECTION('center_axis',(0.866025403784439,0.,-0.5));
#12133=DIRECTION('ref_axis',(0.5,0.,0.866025403784439));
#12134=DIRECTION('',(-0.5,0.,-0.866025403784439));
#12135=DIRECTION('',(0.,-1.,0.));
#12136=DIRECTION('',(0.5,0.,0.866025403784439));
#12137=DIRECTION('',(0.,-1.,0.));
#12138=DIRECTION('center_axis',(1.60246890531964E-16,0.,-1.));
#12139=DIRECTION('ref_axis',(1.,0.,1.60246890531964E-16));
#12140=DIRECTION('',(-1.,0.,-1.60246890531964E-16));
#12141=DIRECTION('',(0.,-1.,0.));
#12142=DIRECTION('',(1.,0.,1.60246890531964E-16));
#12143=DIRECTION('center_axis',(-0.866025403784439,0.,-0.5));
#12144=DIRECTION('ref_axis',(0.5,0.,-0.866025403784439));
#12145=DIRECTION('',(-0.5,0.,0.866025403784439));
#12146=DIRECTION('',(0.,-1.,0.));
#12147=DIRECTION('',(0.5,0.,-0.866025403784439));
#12148=DIRECTION('center_axis',(-0.866025403784439,0.,0.5));
#12149=DIRECTION('ref_axis',(-0.5,0.,-0.866025403784439));
#12150=DIRECTION('',(0.5,0.,0.866025403784439));
#12151=DIRECTION('',(0.,-1.,0.));
#12152=DIRECTION('',(-0.5,0.,-0.866025403784439));
#12153=DIRECTION('center_axis',(-1.60246890531964E-16,0.,1.));
#12154=DIRECTION('ref_axis',(-1.,0.,-1.60246890531964E-16));
#12155=DIRECTION('',(1.,0.,1.60246890531964E-16));
#12156=DIRECTION('',(0.,-1.,0.));
#12157=DIRECTION('',(-1.,0.,-1.60246890531964E-16));
#12158=DIRECTION('center_axis',(0.866025403784439,0.,0.5));
#12159=DIRECTION('ref_axis',(-0.5,0.,0.866025403784439));
#12160=DIRECTION('',(0.5,0.,-0.866025403784439));
#12161=DIRECTION('',(-0.5,0.,0.866025403784439));
#12162=DIRECTION('center_axis',(0.,1.,0.));
#12163=DIRECTION('ref_axis',(1.,0.,0.));
#12164=DIRECTION('center_axis',(0.,-1.,0.));
#12165=DIRECTION('ref_axis',(0.,0.,-1.));
#15317=CARTESIAN_POINT('',(0.,0.,0.));
#15318=CARTESIAN_POINT('Origin',(0.3,0.4,0.));
#15319=CARTESIAN_POINT('',(-0.3,0.4,-3.67394039744206E-17));
#15320=CARTESIAN_POINT('Origin',(0.,0.4,0.));
#15321=CARTESIAN_POINT('Origin',(0.,0.375,0.));
#15322=CARTESIAN_POINT('',(-0.35,0.35,-4.28626379701573E-17));
#15323=CARTESIAN_POINT('Origin',(0.,0.35,0.));
#15324=CARTESIAN_POINT('',(-0.325,0.375,-3.9801020972289E-17));
#15325=CARTESIAN_POINT('Origin',(0.,0.19,0.));
#15326=CARTESIAN_POINT('',(-0.35,0.03,-4.28626379701574E-17));
#15327=CARTESIAN_POINT('Origin',(0.,0.03,0.));
#15328=CARTESIAN_POINT('',(-0.35,0.19,-4.28626379701574E-17));
#15329=CARTESIAN_POINT('Origin',(0.,0.0149999999999999,0.));
#15330=CARTESIAN_POINT('',(-0.32,-3.29597460435593E-17,-3.91886975727153E-17));
#15331=CARTESIAN_POINT('Origin',(0.,0.,0.));
#15332=CARTESIAN_POINT('',(-0.335,0.0149999999999999,-4.10256677714363E-17));
#15333=CARTESIAN_POINT('Origin',(0.22,0.,0.));
#15334=CARTESIAN_POINT('',(-0.22,-6.93889390390723E-18,-2.69422295812418E-17));
#15335=CARTESIAN_POINT('Origin',(0.,0.,0.));
#15336=CARTESIAN_POINT('Origin',(0.,-0.02,0.));
#15337=CARTESIAN_POINT('',(-0.1954,-0.0492,2.39295984553393E-17));
#15338=CARTESIAN_POINT('Origin',(0.,-0.0492,0.));
#15339=CARTESIAN_POINT('',(-0.21,-0.02,-2.57175827820944E-17));
#15340=CARTESIAN_POINT('Origin',(0.,-0.8,0.));
#15341=CARTESIAN_POINT('',(-0.1954,-1.5646,2.39295984553393E-17));
#15342=CARTESIAN_POINT('Origin',(0.,-1.5646,0.));
#15343=CARTESIAN_POINT('',(-0.1954,-0.8,-2.39295984553393E-17));
#15344=CARTESIAN_POINT('Origin',(0.,-1.58,0.));
#15345=CARTESIAN_POINT('',(-0.16,-1.6,-1.95943487863577E-17));
#15346=CARTESIAN_POINT('Origin',(0.,-1.6,0.));
#15347=CARTESIAN_POINT('',(-0.18,-1.58,-2.20436423846524E-17));
#15348=CARTESIAN_POINT('Origin',(0.,-1.6,0.));
#15349=CARTESIAN_POINT('Origin',(0.0866025403784439,-0.4,-0.15));
#15350=CARTESIAN_POINT('',(0.173205080756888,-0.4,0.));
#15351=CARTESIAN_POINT('',(0.0866025403784439,-0.4,-0.15));
#15352=CARTESIAN_POINT('',(0.173205080756888,-0.4,0.));
#15353=CARTESIAN_POINT('',(0.0866025403784439,-0.64,-0.15));
#15354=CARTESIAN_POINT('',(0.0866025403784439,-0.4,-0.15));
#15355=CARTESIAN_POINT('',(0.173205080756888,-0.64,0.));
#15356=CARTESIAN_POINT('',(0.173205080756888,-0.64,0.));
#15357=CARTESIAN_POINT('',(0.173205080756888,-0.4,0.));
#15358=CARTESIAN_POINT('Origin',(-0.0866025403784438,-0.4,-0.15));
#15359=CARTESIAN_POINT('',(-0.0866025403784438,-0.4,-0.15));
#15360=CARTESIAN_POINT('',(0.0866025403784439,-0.4,-0.15));
#15361=CARTESIAN_POINT('',(-0.0866025403784438,-0.64,-0.15));
#15362=CARTESIAN_POINT('',(-0.0866025403784438,-0.4,-0.15));
#15363=CARTESIAN_POINT('',(0.0866025403784439,-0.64,-0.15));
#15364=CARTESIAN_POINT('Origin',(-0.173205080756888,-0.4,-2.77555756156289E-17));
#15365=CARTESIAN_POINT('',(-0.173205080756888,-0.4,-2.12115047744981E-17));
#15366=CARTESIAN_POINT('',(-0.0866025403784438,-0.4,-0.15));
#15367=CARTESIAN_POINT('',(-0.173205080756888,-0.64,-2.77555756156289E-17));
#15368=CARTESIAN_POINT('',(-0.173205080756888,-0.4,-2.12115047744981E-17));
#15369=CARTESIAN_POINT('',(-0.0866025403784438,-0.64,-0.15));
#15370=CARTESIAN_POINT('Origin',(-0.0866025403784439,-0.4,0.15));
#15371=CARTESIAN_POINT('',(-0.0866025403784439,-0.4,0.15));
#15372=CARTESIAN_POINT('',(-0.173205080756888,-0.4,-2.12115047744981E-17));
#15373=CARTESIAN_POINT('',(-0.0866025403784439,-0.64,0.15));
#15374=CARTESIAN_POINT('',(-0.0866025403784439,-0.4,0.15));
#15375=CARTESIAN_POINT('',(-0.173205080756888,-0.64,-2.12115047744981E-17));
#15376=CARTESIAN_POINT('Origin',(0.0866025403784439,-0.4,0.15));
#15377=CARTESIAN_POINT('',(0.0866025403784439,-0.4,0.15));
#15378=CARTESIAN_POINT('',(-0.0866025403784439,-0.4,0.15));
#15379=CARTESIAN_POINT('',(0.0866025403784439,-0.64,0.15));
#15380=CARTESIAN_POINT('',(0.0866025403784439,-0.4,0.15));
#15381=CARTESIAN_POINT('',(-0.0866025403784439,-0.64,0.15));
#15382=CARTESIAN_POINT('Origin',(0.173205080756888,-0.4,0.));
#15383=CARTESIAN_POINT('',(0.0866025403784439,-0.4,0.15));
#15384=CARTESIAN_POINT('',(0.0866025403784439,-0.64,0.15));
#15385=CARTESIAN_POINT('Origin',(0.,-0.4,-2.77555756156289E-17));
#15386=CARTESIAN_POINT('Origin',(0.,-0.64,-2.77555756156289E-17));
#17223=UNCERTAINTY_MEASURE_WITH_UNIT(LENGTH_MEASURE(0.001),#17323,
'DISTANCE_ACCURACY_VALUE',
'Maximum model space distance between geometric entities at asserted c
onnectivities');
#17261=UNCERTAINTY_MEASURE_WITH_UNIT(LENGTH_MEASURE(0.001),#17323,
'DISTANCE_ACCURACY_VALUE',
'Maximum model space distance between geometric entities at asserted c
onnectivities');
#17284=(
GEOMETRIC_REPRESENTATION_CONTEXT(3)
GLOBAL_UNCERTAINTY_ASSIGNED_CONTEXT((#17223))
GLOBAL_UNIT_ASSIGNED_CONTEXT((#17323,#17325,#17326))
REPRESENTATION_CONTEXT('','3D')
);
#17322=(
GEOMETRIC_REPRESENTATION_CONTEXT(3)
GLOBAL_UNCERTAINTY_ASSIGNED_CONTEXT((#17261))
GLOBAL_UNIT_ASSIGNED_CONTEXT((#17323,#17325,#17326))
REPRESENTATION_CONTEXT('','3D')
);
#17323=(
LENGTH_UNIT()
NAMED_UNIT(*)
SI_UNIT(.CENTI.,.METRE.)
);
#17325=(
NAMED_UNIT(*)
PLANE_ANGLE_UNIT()
SI_UNIT($,.RADIAN.)
);
#17326=(
NAMED_UNIT(*)
SI_UNIT($,.STERADIAN.)
SOLID_ANGLE_UNIT()
);
#17349=SHAPE_DEFINITION_REPRESENTATION(#17411,#17580);
#17411=PRODUCT_DEFINITION_SHAPE('',$,#17641);
#17580=SHAPE_REPRESENTATION('',(#10150),#17284);
#17618=PRODUCT_DEFINITION_CONTEXT('part definition',#17800,'design');
#17641=PRODUCT_DEFINITION('Cap Screw - M4x16','Cap Screw - M4x16',#17701,
#17618);
#17701=PRODUCT_DEFINITION_FORMATION('',$,#17824);
#17800=APPLICATION_CONTEXT(
'Core Data for Automotive Mechanical Design Process');
#17801=PRODUCT_CONTEXT('part definition',#17800,'mechanical');
#17824=PRODUCT('Cap Screw - M4x16','Cap Screw - M4x16',
'Cap Screw - M4x16',(#17801));
#17932=COLOUR_RGB('Black',0.12,0.14,0.17);
#17933=FILL_AREA_STYLE_COLOUR('',#17932);
#17934=FILL_AREA_STYLE('',(#17933));
#17935=SURFACE_STYLE_FILL_AREA(#17934);
#17936=SURFACE_SIDE_STYLE('',(#17935));
#17937=SURFACE_STYLE_USAGE(.BOTH.,#17936);
#17938=PRESENTATION_STYLE_ASSIGNMENT((#17937));
ENDSEC;
END-ISO-10303-21;
